ISO-10303-21;
HEADER;
FILE_DESCRIPTION (('STEP AP203'),
    '1' );
FILE_NAME ('Aloris-BXA-Wedge-L.step',
    '2026-10-07T20:09:13',
    ( '' ),
    ( '' ),
    'SwSTEP 2.0',
    'SolidWorks 2024',
    '' );
FILE_SCHEMA (( 'AUTOMOTIVE_DESIGN' ));
ENDSEC;

DATA;
#42=DIRECTION ( 'NONE',  ( -0.000000000000000000, 0.000000000000000000, 1.000000000000000000 ) ) ;
#134=FACE_OUTER_BOUND ( 'NONE', #4569, .T. ) ;
#208=VECTOR ( 'NONE', #13056, 39.37007874015748854 ) ;
#244=CLOSED_SHELL ( 'NONE', ( #18887, #14949, #5630, #5410, #4548, #13026, #18679, #3074, #17557, #11622, #8845, #6138, #15005, #14422, #9769, #4119, #5737 ) ) ;
#339=EDGE_LOOP ( 'NONE', ( #18728, #8488, #19395, #1831 ) ) ;
#380=CARTESIAN_POINT ( 'NONE',  ( -0.09435543239133792337, 4.559812086079793048, -2.854670964936879329 ) ) ;
#408=CARTESIAN_POINT ( 'NONE',  ( -0.5116234456863258950, 2.853030769935284816, -2.640781157734872320 ) ) ;
#447=ORIENTED_EDGE ( 'NONE', *, *, #19474, .T. ) ;
#496=ORIENTED_EDGE ( 'NONE', *, *, #14555, .F. ) ;
#574=VECTOR ( 'NONE', #6340, 39.37007874015748143 ) ;
#577=DIMENSIONAL_EXPONENTS ( 1.000000000000000000, 0.000000000000000000, 0.000000000000000000, 0.000000000000000000, 0.000000000000000000, 0.000000000000000000, 0.000000000000000000 ) ;
#604=LINE ( 'NONE', #22912, #21836 ) ;
#620=EDGE_CURVE ( 'NONE', #3437, #18019, #10851, .T. ) ;
#621=CARTESIAN_POINT ( 'NONE',  ( -0.09435543239133792337, 1.041821957232212270, -2.854670964936879329 ) ) ;
#627=CARTESIAN_POINT ( 'NONE',  ( -0.1060554323913378977, 4.559812086079793048, -2.874935959385435336 ) ) ;
#644=VERTEX_POINT ( 'NONE', #18759 ) ;
#651=ORIENTED_EDGE ( 'NONE', *, *, #19743, .T. ) ;
#673=ORIENTED_EDGE ( 'NONE', *, *, #14315, .T. ) ;
#675=ORIENTED_EDGE ( 'NONE', *, *, #13849, .T. ) ;
#793=ORIENTED_EDGE ( 'NONE', *, *, #11721, .F. ) ;
#819=ORIENTED_EDGE ( 'NONE', *, *, #2364, .F. ) ;
#862=CARTESIAN_POINT ( 'NONE',  ( -0.1868639192671614491, 4.559812086079793048, -3.228500364337123951 ) ) ;
#865=DIRECTION ( 'NONE',  ( -0.4985709748471500169, -0.07555085810113110201, -0.8635502596144276621 ) ) ;
#877=ORIENTED_EDGE ( 'NONE', *, *, #22131, .F. ) ;
#900=LINE ( 'NONE', #17372, #14856 ) ;
#916=FACE_OUTER_BOUND ( 'NONE', #339, .T. ) ;
#1152=EDGE_LOOP ( 'NONE', ( #12346, #17673, #18185, #7554 ) ) ;
#1175=LINE ( 'NONE', #3006, #7710 ) ;
#1208=MANIFOLD_SOLID_BREP ( 'VarFillet1', #244 ) ;
#1263=ORIENTED_EDGE ( 'NONE', *, *, #11423, .T. ) ;
#1324=VECTOR ( 'NONE', #23404, 39.37007874015748854 ) ;
#1329=FACE_OUTER_BOUND ( 'NONE', #8390, .T. ) ;
#1359=EDGE_LOOP ( 'NONE', ( #877, #5213, #496, #3710, #14056, #447 ) ) ;
#1366=LENGTH_MEASURE_WITH_UNIT ( LENGTH_MEASURE( 0.02539999999999999897 ), #16604 );
#1411=APPLICATION_CONTEXT ( 'configuration controlled 3d designs of mechanical parts and assemblies' ) ;
#1441=LINE ( 'NONE', #6682, #16065 ) ;
#1460=CARTESIAN_POINT ( 'NONE',  ( -0.1166234456863257940, 4.111524471938507119, -2.868834514064774854 ) ) ;
#1515=( BOUNDED_SURFACE ( )  B_SPLINE_SURFACE ( 2, 3, ( 
 ( #22481, #5776, #8957, #5297, #20178, #3465, #10916, #1639, #9074, #23940 ),
 ( #22949, #22839, #17474, #9807, #408, #20891, #17120, #13350, #13712, #9925 ),
 ( #2606, #9558, #8198, #8075, #15411, #5890, #16992, #11758, #21132, #13476 ) ),
 .UNSPECIFIED., .F., .F., .T. ) 
 B_SPLINE_SURFACE_WITH_KNOTS ( ( 3, 3 ),
 ( 4, 3, 3, 4 ),
 ( 0.000000000000000000, 1.000000000000000000 ),
 ( 0.01132290749860156119, 0.02432858112762277536, 0.08935694927272853916, 0.1023626229017496753 ),
 .UNSPECIFIED. ) 
 GEOMETRIC_REPRESENTATION_ITEM ( )  RATIONAL_B_SPLINE_SURFACE ( (
 ( 1.000000000000000000, 1.000000000000000000, 1.000000000000000000, 1.000000000000000000, 1.000000000000000000, 1.000000000000000000, 1.000000000000000000, 1.000000000000000000, 1.000000000000000000, 1.000000000000000000),
 ( 0.4999999999999997780, 0.4999999999999997780, 0.4999999999999997780, 0.4999999999999997780, 0.4999999999999997780, 0.4999999999999997780, 0.4999999999999997780, 0.4999999999999997780, 0.4999999999999997780, 0.4999999999999997780),
 ( 1.000000000000000000, 1.000000000000000000, 1.000000000000000000, 1.000000000000000000, 1.000000000000000000, 1.000000000000000000, 1.000000000000000000, 1.000000000000000000, 1.000000000000000000, 1.000000000000000000) ) ) 
 REPRESENTATION_ITEM ( '' )  SURFACE ( )  );
#1520=ORIENTED_EDGE ( 'NONE', *, *, #14315, .F. ) ;
#1571=DIRECTION ( 'NONE',  ( 0.4999999999999942268, 0.000000000000000000, 0.8660254037844420383 ) ) ;
#1639=CARTESIAN_POINT ( 'NONE',  ( -0.5116234456863258950, 4.730490217694244492, -2.819759741183656132 ) ) ;
#1646=ORIENTED_EDGE ( 'NONE', *, *, #19474, .F. ) ;
#1678=DIRECTION ( 'NONE',  ( 0.000000000000000000, -0.9961946980917454342, 0.08715574274765833240 ) ) ;
#1729=ORIENTED_EDGE ( 'NONE', *, *, #1812, .T. ) ;
#1730=ORIENTED_EDGE ( 'NONE', *, *, #2615, .T. ) ;
#1812=EDGE_CURVE ( 'NONE', #16762, #4265, #19042, .T. ) ;
#1820=ORIENTED_EDGE ( 'NONE', *, *, #21215, .F. ) ;
#1831=ORIENTED_EDGE ( 'NONE', *, *, #16016, .T. ) ;
#1844=ORIENTED_EDGE ( 'NONE', *, *, #7479, .F. ) ;
#1845=ORIENTED_EDGE ( 'NONE', *, *, #3639, .T. ) ;
#2059=ORIENTED_EDGE ( 'NONE', *, *, #21038, .F. ) ;
#2138=( GEOMETRIC_REPRESENTATION_CONTEXT ( 3 ) GLOBAL_UNCERTAINTY_ASSIGNED_CONTEXT ( ( #17531 ) ) GLOBAL_UNIT_ASSIGNED_CONTEXT ( ( #20141, #6852, #16366 ) ) REPRESENTATION_CONTEXT ( 'NONE', 'WORKASPACE' ) );
#2149=VECTOR ( 'NONE', #3040, 39.37007874015748854 ) ;
#2243=ORIENTED_EDGE ( 'NONE', *, *, #7426, .T. ) ;
#2291=CARTESIAN_POINT ( 'NONE',  ( -0.1868639192671616156, 4.559812086079793048, -3.228500364337124395 ) ) ;
#2293=CARTESIAN_POINT ( 'NONE',  ( -0.05329418186028045401, 1.034028482145805672, -2.997150792794772922 ) ) ;
#2339=EDGE_CURVE ( 'NONE', #5324, #9833, #14882, .T. ) ;
#2364=EDGE_CURVE ( 'NONE', #18643, #2744, #14516, .T. ) ;
#2429=CARTESIAN_POINT ( 'NONE',  ( 0.000000000000000000, 4.559812086079793048, 0.000000000000000000 ) ) ;
#2535=VERTEX_POINT ( 'NONE', #17777 ) ;
#2565=VECTOR ( 'NONE', #13692, 39.37007874015748143 ) ;
#2606=CARTESIAN_POINT ( 'NONE',  ( -0.4516234456863258973, 1.487605717019675700, -2.675422173886249588 ) ) ;
#2615=EDGE_CURVE ( 'NONE', #3437, #644, #21436, .T. ) ;
#2739=VERTEX_POINT ( 'NONE', #13890 ) ;
#2744=VERTEX_POINT ( 'NONE', #15593 ) ;
#2812=ORIENTED_EDGE ( 'NONE', *, *, #2339, .T. ) ;
#3006=CARTESIAN_POINT ( 'NONE',  ( 1.078523662826197160, 4.111524471938507119, -0.8231847808846625147 ) ) ;
#3010=EDGE_CURVE ( 'NONE', #3821, #21597, #19550, .T. ) ;
#3040=DIRECTION ( 'NONE',  ( -0.8660254037844434816, -1.483353696775904202E-31, 0.4999999999999913403 ) ) ;
#3068=EDGE_CURVE ( 'NONE', #4326, #19937, #6505, .T. ) ;
#3074=ADVANCED_FACE ( 'NONE', ( #14187 ), #21384, .T. ) ;
#3081=ORIENTED_EDGE ( 'NONE', *, *, #17650, .F. ) ;
#3299=DIRECTION ( 'NONE',  ( 0.4999999999999916178, 6.654928120984803295E-16, 0.8660254037844433705 ) ) ;
#3409=CARTESIAN_POINT ( 'NONE',  ( -0.5116234456863258950, 4.111524471938507119, -2.845780280100676851 ) ) ;
#3437=VERTEX_POINT ( 'NONE', #9485 ) ;
#3443=PLANE ( 'NONE',  #15739 ) ;
#3465=CARTESIAN_POINT ( 'NONE',  ( -0.5116234456863258950, 3.706421428007538488, -2.785118725032278419 ) ) ;
#3470=CARTESIAN_POINT ( 'NONE',  ( 0.3860879860166684940, 4.111524471938507119, -2.831872695974971599 ) ) ;
#3497=EDGE_CURVE ( 'NONE', #10744, #3821, #15101, .T. ) ;
#3512=LINE ( 'NONE', #9118, #4637 ) ;
#3639=EDGE_CURVE ( 'NONE', #23261, #3437, #1175, .T. ) ;
#3710=ORIENTED_EDGE ( 'NONE', *, *, #3497, .T. ) ;
#3784=EDGE_CURVE ( 'NONE', #16705, #4879, #10333, .T. ) ;
#3821=VERTEX_POINT ( 'NONE', #7151 ) ;
#3989=DIRECTION ( 'NONE',  ( 0.000000000000000000, 1.000000000000000000, 0.000000000000000000 ) ) ;
#4023=CARTESIAN_POINT ( 'NONE',  ( -0.4366234456863259394, 1.999640111863030478, -2.684082427924094016 ) ) ;
#4052=CARTESIAN_POINT ( 'NONE',  ( -0.3616234456863257618, 4.559812086079793048, -2.727383698113316157 ) ) ;
#4119=ADVANCED_FACE ( 'NONE', ( #5006 ), #21363, .F. ) ;
#4265=VERTEX_POINT ( 'NONE', #16714 ) ;
#4283=FACE_OUTER_BOUND ( 'NONE', #1359, .T. ) ;
#4293=ORIENTED_EDGE ( 'NONE', *, *, #16381, .F. ) ;
#4322=AXIS2_PLACEMENT_3D ( 'NONE', #18216, #16393, #19675 ) ;
#4326=VERTEX_POINT ( 'NONE', #15014 ) ;
#4430=ORIENTED_EDGE ( 'NONE', *, *, #620, .T. ) ;
#4532=EDGE_CURVE ( 'NONE', #9492, #2739, #15077, .T. ) ;
#4548=ADVANCED_FACE ( 'NONE', ( #12204 ), #10365, .T. ) ;
#4569=EDGE_LOOP ( 'NONE', ( #17878, #9998, #8657, #1820 ) ) ;
#4618=DIRECTION ( 'NONE',  ( 0.4999999999999916178, 0.000000000000000000, 0.8660254037844433705 ) ) ;
#4637=VECTOR ( 'NONE', #16566, 39.37007874015748143 ) ;
#4693=DIRECTION ( 'NONE',  ( 0.4985709748471340297, 0.07555085810113193467, 0.8635502596144368770 ) ) ;
#4829=CARTESIAN_POINT ( 'NONE',  ( -0.5116234456863258950, 3.706421428007538488, -2.785118725032278419 ) ) ;
#4861=CARTESIAN_POINT ( 'NONE',  ( 0.3530939849935350594, 1.999640111863030478, -2.889019982092019045 ) ) ;
#4879=VERTEX_POINT ( 'NONE', #11806 ) ;
#4913=LINE ( 'NONE', #20275, #7553 ) ;
#4915=CARTESIAN_POINT ( 'NONE',  ( 0.2730879860166738338, 4.111524471938507119, -3.027594437230249902 ) ) ;
#4930=CARTESIAN_POINT ( 'NONE',  ( -0.02441201398332129568, 4.111524471938507119, -3.542879552481994043 ) ) ;
#4933=LINE ( 'NONE', #8711, #16363 ) ;
#4946=CARTESIAN_POINT ( 'NONE',  ( 0.3003475124358450099, 4.111524471938507119, -3.730379552481990491 ) ) ;
#5006=FACE_OUTER_BOUND ( 'NONE', #16300, .T. ) ;
#5028=DIRECTION ( 'NONE',  ( 0.000000000000000000, 0.000000000000000000, 1.000000000000000000 ) ) ;
#5124=DIRECTION ( 'NONE',  ( -3.327464060492345934E-16, 1.000000000000000000, -5.763336813132313106E-16 ) ) ;
#5139=ORIENTED_EDGE ( 'NONE', *, *, #23240, .T. ) ;
#5213=ORIENTED_EDGE ( 'NONE', *, *, #7535, .F. ) ;
#5274=DIRECTION ( 'NONE',  ( 0.000000000000000000, -5.763336813132313106E-16, -1.000000000000000000 ) ) ;
#5297=CARTESIAN_POINT ( 'NONE',  ( -0.5116234456863258950, 1.999640111863030478, -2.727383698113316157 ) ) ;
#5324=VERTEX_POINT ( 'NONE', #4930 ) ;
#5393=CARTESIAN_POINT ( 'NONE',  ( 0.3860879860166717692, 1.999640111863030700, -2.647106755790660682 ) ) ;
#5410=ADVANCED_FACE ( 'NONE', ( #18106 ), #23573, .T. ) ;
#5456=VECTOR ( 'NONE', #15215, 39.37007874015748854 ) ;
#5485=ORIENTED_EDGE ( 'NONE', *, *, #7535, .T. ) ;
#5532=ORIENTED_EDGE ( 'NONE', *, *, #7291, .T. ) ;
#5557=CARTESIAN_POINT ( 'NONE',  ( -0.1166234456863257940, 4.111524471938507119, -2.802594437230254254 ) ) ;
#5630=ADVANCED_FACE ( 'NONE', ( #7488 ), #15057, .T. ) ;
#5649=DIRECTION ( 'NONE',  ( -0.8660254037844526964, 0.000000000000000000, 0.4999999999999756306 ) ) ;
#5736=CARTESIAN_POINT ( 'NONE',  ( -0.4116234456863256952, 2.853030769935287037, -2.698516184653834582 ) ) ;
#5737=ADVANCED_FACE ( 'NONE', ( #21998 ), #1515, .T. ) ;
#5776=CARTESIAN_POINT ( 'NONE',  ( -0.5116234456863258950, 1.658283848634127366, -2.715836692729523438 ) ) ;
#5817=DIRECTION ( 'NONE',  ( 0.03777542905056541916, -0.9971419496943164651, 0.06542896239329260011 ) ) ;
#5848=CARTESIAN_POINT ( 'NONE',  ( -0.4366234456863259394, 1.999640111863030478, -2.684082427924094016 ) ) ;
#5854=AXIS2_PLACEMENT_3D ( 'NONE', #7529, #14864, #11074 ) ;
#5890=CARTESIAN_POINT ( 'NONE',  ( -0.3866234456863258395, 3.706421428007538488, -2.712949941383575592 ) ) ;
#5959=CARTESIAN_POINT ( 'NONE',  ( -0.3616234456863257618, 4.559812086079793048, -2.727383698113316157 ) ) ;
#6138=ADVANCED_FACE ( 'NONE', ( #134 ), #9651, .T. ) ;
#6242=CARTESIAN_POINT ( 'NONE',  ( -0.5116234456863258950, 1.999640111863030478, -2.640781157734871876 ) ) ;
#6337=EDGE_CURVE ( 'NONE', #8276, #18019, #21044, .T. ) ;
#6340=DIRECTION ( 'NONE',  ( 0.000000000000000000, 1.000000000000000000, 0.000000000000000000 ) ) ;
#6400=VECTOR ( 'NONE', #5649, 39.37007874015748143 ) ;
#6505=LINE ( 'NONE', #4915, #23629 ) ;
#6623=AXIS2_PLACEMENT_3D ( 'NONE', #9176, #14801, #18563 ) ;
#6627=FACE_OUTER_BOUND ( 'NONE', #21211, .T. ) ;
#6642=CARTESIAN_POINT ( 'NONE',  ( 0.2730879860166738338, 4.111524471938507119, -3.027594437230249902 ) ) ;
#6648=ORIENTED_EDGE ( 'NONE', *, *, #11423, .F. ) ;
#6649=ORIENTED_EDGE ( 'NONE', *, *, #7479, .T. ) ;
#6682=CARTESIAN_POINT ( 'NONE',  ( 0.3860879860166684940, 4.111524471938507119, -2.831872695974971599 ) ) ;
#6763=EDGE_LOOP ( 'NONE', ( #22419, #6648, #20269, #16159 ) ) ;
#6852=( NAMED_UNIT ( * ) PLANE_ANGLE_UNIT ( ) SI_UNIT ( $, .RADIAN. ) );
#7008=ORIENTED_EDGE ( 'NONE', *, *, #12445, .T. ) ;
#7066=VECTOR ( 'NONE', #9256, 39.37007874015748143 ) ;
#7073=LINE ( 'NONE', #1460, #7066 ) ;
#7118=LINE ( 'NONE', #8114, #8532 ) ;
#7151=CARTESIAN_POINT ( 'NONE',  ( -0.1698811246234971650, 4.111524471938507119, -3.199085301159788841 ) ) ;
#7270=CARTESIAN_POINT ( 'NONE',  ( -0.09435543239133792337, 4.559812086079793048, -2.854670964936879329 ) ) ;
#7291=EDGE_CURVE ( 'NONE', #8965, #2744, #19576, .T. ) ;
#7394=LINE ( 'NONE', #5557, #19850 ) ;
#7396=ADVANCED_BREP_SHAPE_REPRESENTATION ( '', ( #1208, #9127 ), #2138 ) ;
#7426=EDGE_CURVE ( 'NONE', #20410, #19381, #7118, .T. ) ;
#7479=EDGE_CURVE ( 'NONE', #4265, #10744, #21904, .T. ) ;
#7488=FACE_OUTER_BOUND ( 'NONE', #6763, .T. ) ;
#7529=CARTESIAN_POINT ( 'NONE',  ( -0.5116234456863258950, 1.041821957232212270, -2.640781157734871876 ) ) ;
#7535=EDGE_CURVE ( 'NONE', #9500, #23062, #3512, .T. ) ;
#7553=VECTOR ( 'NONE', #5028, 39.37007874015748143 ) ;
#7554=ORIENTED_EDGE ( 'NONE', *, *, #3784, .T. ) ;
#7565=ORIENTED_EDGE ( 'NONE', *, *, #9690, .F. ) ;
#7576=DIRECTION ( 'NONE',  ( 0.5000000000000003331, 0.000000000000000000, 0.8660254037844383745 ) ) ;
#7599=LINE ( 'NONE', #22348, #12660 ) ;
#7710=VECTOR ( 'NONE', #17639, 39.37007874015747433 ) ;
#7736=ORIENTED_EDGE ( 'NONE', *, *, #13075, .F. ) ;
#7804=CARTESIAN_POINT ( 'NONE',  ( -0.001863919267159286786, 4.111524471938507119, -2.908070964936878333 ) ) ;
#7805=ORIENTED_EDGE ( 'NONE', *, *, #16175, .T. ) ;
#7837=LINE ( 'NONE', #20763, #6400 ) ;
#7866=ORIENTED_EDGE ( 'NONE', *, *, #11555, .F. ) ;
#8033=VECTOR ( 'NONE', #10972, 39.37007874015748143 ) ;
#8075=CARTESIAN_POINT ( 'NONE',  ( -0.4366234456863258839, 1.999640111863030478, -2.684082427924094016 ) ) ;
#8100=ORIENTED_EDGE ( 'NONE', *, *, #3010, .F. ) ;
#8114=CARTESIAN_POINT ( 'NONE',  ( -0.1166234456863257940, 1.999640111863030478, -2.802594437230252922 ) ) ;
#8141=DIRECTION ( 'NONE',  ( -0.8660254037844382635, 0.000000000000000000, 0.5000000000000004441 ) ) ;
#8155=ORIENTED_EDGE ( 'NONE', *, *, #19743, .F. ) ;
#8198=CARTESIAN_POINT ( 'NONE',  ( -0.4416234456863259439, 1.828961980248579033, -2.681195676578145726 ) ) ;
#8264=EDGE_CURVE ( 'NONE', #19381, #9492, #13339, .T. ) ;
#8276=VERTEX_POINT ( 'NONE', #4052 ) ;
#8345=PLANE ( 'NONE',  #21420 ) ;
#8377=ORIENTED_EDGE ( 'NONE', *, *, #14555, .T. ) ;
#8390=EDGE_LOOP ( 'NONE', ( #11490, #15791, #20808, #9616 ) ) ;
#8488=ORIENTED_EDGE ( 'NONE', *, *, #7291, .F. ) ;
#8489=CARTESIAN_POINT ( 'NONE',  ( -0.5116234456863258950, 1.999640111863030256, -2.727383698113316157 ) ) ;
#8516=EDGE_LOOP ( 'NONE', ( #14323, #3081, #1520, #2059 ) ) ;
#8532=VECTOR ( 'NONE', #5274, 39.37007874015748143 ) ;
#8541=LINE ( 'NONE', #15983, #1324 ) ;
#8576=DIRECTION ( 'NONE',  ( 0.8660254037844432595, 0.000000000000000000, -0.4999999999999916733 ) ) ;
#8657=ORIENTED_EDGE ( 'NONE', *, *, #1812, .F. ) ;
#8711=CARTESIAN_POINT ( 'NONE',  ( 0.3060819870398079900, 1.999640111863030478, -2.785681210928895535 ) ) ;
#8791=PRODUCT_DEFINITION ( 'UNKNOWN', '', #11526, #21188 ) ;
#8819=DIRECTION ( 'NONE',  ( 0.000000000000000000, -5.763336813132313106E-16, -1.000000000000000000 ) ) ;
#8845=ADVANCED_FACE ( 'NONE', ( #1329 ), #21923, .T. ) ;
#8854=VECTOR ( 'NONE', #8576, 39.37007874015748143 ) ;
#8875=DIRECTION ( 'NONE',  ( 0.000000000000000000, -0.9961946980917454342, 0.08715574274765833240 ) ) ;
#8917=PLANE ( 'NONE',  #9493 ) ;
#8918=EDGE_LOOP ( 'NONE', ( #7736, #19724, #651, #18973 ) ) ;
#8935=CARTESIAN_POINT ( 'NONE',  ( 0.3003475124358450099, 4.111524471938507119, -3.730379552481990491 ) ) ;
#8957=CARTESIAN_POINT ( 'NONE',  ( -0.5116234456863258950, 1.828961980248579033, -2.721610195421419576 ) ) ;
#8965=VERTEX_POINT ( 'NONE', #16328 ) ;
#8976=VECTOR ( 'NONE', #22670, 39.37007874015748143 ) ;
#9033=ORIENTED_EDGE ( 'NONE', *, *, #22131, .T. ) ;
#9074=CARTESIAN_POINT ( 'NONE',  ( -0.5116234456863258950, 4.901168349308694161, -2.825533243875552269 ) ) ;
#9118=CARTESIAN_POINT ( 'NONE',  ( -0.5116234456863258950, 5.163786281674128453, -3.093841259513817388 ) ) ;
#9127=AXIS2_PLACEMENT_3D ( 'NONE', #15878, #23181, #23294 ) ;
#9146=LINE ( 'NONE', #16590, #8976 ) ;
#9176=CARTESIAN_POINT ( 'NONE',  ( -0.001863919267159286786, 1.041821957232212270, -2.908070964936878333 ) ) ;
#9195=ORIENTED_EDGE ( 'NONE', *, *, #17515, .T. ) ;
#9224=EDGE_LOOP ( 'NONE', ( #16031, #13979, #12073, #18882, #19458, #4430 ) ) ;
#9241=CARTESIAN_POINT ( 'NONE',  ( -1.172879095217528311, 4.111524471938507119, -2.231985037876813127 ) ) ;
#9256=DIRECTION ( 'NONE',  ( 0.000000000000000000, 1.000000000000000000, 0.000000000000000000 ) ) ;
#9408=CARTESIAN_POINT ( 'NONE',  ( 1.171015175950385068, 4.111524471938507119, -0.8765847808846783940 ) ) ;
#9485=CARTESIAN_POINT ( 'NONE',  ( -0.1060554323913378977, 4.111524471938507119, -2.874935959385435336 ) ) ;
#9492=VERTEX_POINT ( 'NONE', #11055 ) ;
#9493=AXIS2_PLACEMENT_3D ( 'NONE', #16359, #18540, #18422 ) ;
#9500=VERTEX_POINT ( 'NONE', #21899 ) ;
#9529=DIRECTION ( 'NONE',  ( 0.8660254037844443697, 0.000000000000000000, -0.4999999999999901745 ) ) ;
#9558=CARTESIAN_POINT ( 'NONE',  ( -0.4466234456863258928, 1.658283848634127366, -2.678308925232197879 ) ) ;
#9616=ORIENTED_EDGE ( 'NONE', *, *, #620, .F. ) ;
#9651=PLANE ( 'NONE',  #17471 ) ;
#9674=APPLICATION_CONTEXT ( 'configuration controlled 3d designs of mechanical parts and assemblies' ) ;
#9677=AXIS2_PLACEMENT_3D ( 'NONE', #13001, #18465, #42 ) ;
#9690=EDGE_CURVE ( 'NONE', #19937, #644, #7394, .T. ) ;
#9736=EDGE_LOOP ( 'NONE', ( #14598, #673, #17527, #5139, #1729, #6649, #8377 ) ) ;
#9769=ADVANCED_FACE ( 'NONE', ( #12740 ), #11017, .T. ) ;
#9807=CARTESIAN_POINT ( 'NONE',  ( -0.5116234456863258950, 1.999640111863030478, -2.640781157734872320 ) ) ;
#9833=VERTEX_POINT ( 'NONE', #18205 ) ;
#9871=FACE_OUTER_BOUND ( 'NONE', #9736, .T. ) ;
#9897=DIRECTION ( 'NONE',  ( 0.4999999999999901745, -0.000000000000000000, 0.8660254037844443697 ) ) ;
#9925=CARTESIAN_POINT ( 'NONE',  ( -0.5116234456863258950, 5.071846480923145606, -2.640781157734872320 ) ) ;
#9994=DIRECTION ( 'NONE',  ( -0.000000000000000000, 1.000000000000000000, 0.000000000000000000 ) ) ;
#9998=ORIENTED_EDGE ( 'NONE', *, *, #16381, .T. ) ;
#10029=CARTESIAN_POINT ( 'NONE',  ( -0.09435543239133792337, 4.111524471938507119, -2.854670964936879329 ) ) ;
#10032=DIRECTION ( 'NONE',  ( -0.8660254037844432595, 0.000000000000000000, 0.4999999999999916733 ) ) ;
#10333=LINE ( 'NONE', #4946, #11602 ) ;
#10353=CARTESIAN_POINT ( 'NONE',  ( -1.184579095217545452, 4.111524471938507119, -2.252250032325342488 ) ) ;
#10365=PLANE ( 'NONE',  #23265 ) ;
#10396=DIRECTION ( 'NONE',  ( -0.4999999999999929501, 0.000000000000000000, -0.8660254037844425934 ) ) ;
#10544=CARTESIAN_POINT ( 'NONE',  ( -0.5116234456863258950, 1.999640111863030256, -2.845780280100675963 ) ) ;
#10558=DIRECTION ( 'NONE',  ( 0.8660254037844435926, 0.000000000000000000, -0.4999999999999914513 ) ) ;
#10650=FACE_OUTER_BOUND ( 'NONE', #14958, .T. ) ;
#10677=VECTOR ( 'NONE', #18413, 39.37007874015748143 ) ;
#10739=CARTESIAN_POINT ( 'NONE',  ( -0.02441201398332129568, 4.111524471938507119, -3.542879552481994043 ) ) ;
#10744=VERTEX_POINT ( 'NONE', #862 ) ;
#10788=PLANE ( 'NONE',  #4322 ) ;
#10795=ORIENTED_EDGE ( 'NONE', *, *, #19305, .T. ) ;
#10802=VECTOR ( 'NONE', #21937, 39.37007874015748854 ) ;
#10851=LINE ( 'NONE', #23867, #8033 ) ;
#10859=DIRECTION ( 'NONE',  ( -0.000000000000000000, 0.000000000000000000, 1.000000000000000000 ) ) ;
#10873=CARTESIAN_POINT ( 'NONE',  ( 0.3003475124358454540, 1.999640111863030256, -3.545613612297686679 ) ) ;
#10916=CARTESIAN_POINT ( 'NONE',  ( -0.5116234456863258950, 4.559812086079793048, -2.813986238491759551 ) ) ;
#10972=DIRECTION ( 'NONE',  ( 0.000000000000000000, 1.000000000000000000, 0.000000000000000000 ) ) ;
#10988=LINE ( 'NONE', #20483, #10677 ) ;
#11017=PLANE ( 'NONE',  #6623 ) ;
#11055=CARTESIAN_POINT ( 'NONE',  ( -0.4366234456863259394, 1.999640111863030478, -2.684082427924094016 ) ) ;
#11074=DIRECTION ( 'NONE',  ( 0.8660254037844382635, 0.000000000000000000, -0.5000000000000004441 ) ) ;
#11095=PLANE ( 'NONE',  #15993 ) ;
#11243=LINE ( 'NONE', #9408, #15231 ) ;
#11338=FACE_OUTER_BOUND ( 'NONE', #22812, .T. ) ;
#11389=VECTOR ( 'NONE', #3989, 39.37007874015748143 ) ;
#11423=EDGE_CURVE ( 'NONE', #19937, #20410, #900, .T. ) ;
#11465=VERTEX_POINT ( 'NONE', #15897 ) ;
#11490=ORIENTED_EDGE ( 'NONE', *, *, #3639, .F. ) ;
#11526=PRODUCT_DEFINITION_FORMATION_WITH_SPECIFIED_SOURCE ( 'ANY', '', #18099, .NOT_KNOWN. ) ;
#11555=EDGE_CURVE ( 'NONE', #2739, #23062, #17729, .T. ) ;
#11602=VECTOR ( 'NONE', #17760, 39.37007874015748143 ) ;
#11622=ADVANCED_FACE ( 'NONE', ( #6627 ), #10788, .F. ) ;
#11714=CARTESIAN_POINT ( 'NONE',  ( -0.3866234456863257840, 3.706421428007541596, -2.712949941383575592 ) ) ;
#11721=EDGE_CURVE ( 'NONE', #5324, #16705, #604, .T. ) ;
#11758=CARTESIAN_POINT ( 'NONE',  ( -0.3566234456863258129, 4.730490217694244492, -2.730270449459264004 ) ) ;
#11806=CARTESIAN_POINT ( 'NONE',  ( 0.3003475124358454540, 1.999640111863030256, -3.545613612297686679 ) ) ;
#11810=EDGE_LOOP ( 'NONE', ( #21875, #19814, #16010, #1263 ) ) ;
#12002=CARTESIAN_POINT ( 'NONE',  ( -0.1166234456863257940, 1.999640111863030478, -2.617828497045949110 ) ) ;
#12073=ORIENTED_EDGE ( 'NONE', *, *, #8264, .F. ) ;
#12157=MECHANICAL_CONTEXT ( 'NONE', #9674, 'mechanical' ) ;
#12161=DIRECTION ( 'NONE',  ( 0.8660254037844526964, 0.000000000000000000, -0.4999999999999757416 ) ) ;
#12204=FACE_OUTER_BOUND ( 'NONE', #8918, .T. ) ;
#12266=ORIENTED_EDGE ( 'NONE', *, *, #12445, .F. ) ;
#12281=VERTEX_POINT ( 'NONE', #3470 ) ;
#12299=CARTESIAN_POINT ( 'NONE',  ( -0.5116234456863258950, 4.559812086079793048, -2.813986238491759551 ) ) ;
#12346=ORIENTED_EDGE ( 'NONE', *, *, #19305, .F. ) ;
#12440=VECTOR ( 'NONE', #19715, 39.37007874015748854 ) ;
#12445=EDGE_CURVE ( 'NONE', #3821, #17621, #11243, .T. ) ;
#12485=ORIENTED_EDGE ( 'NONE', *, *, #20194, .F. ) ;
#12576=CARTESIAN_POINT ( 'NONE',  ( -0.3066867353193226120, 1.999640111863030700, -2.247133083939565790 ) ) ;
#12590=DIRECTION ( 'NONE',  ( 0.000000000000000000, 5.763336813132313106E-16, 1.000000000000000000 ) ) ;
#12660=VECTOR ( 'NONE', #14928, 39.37007874015748143 ) ;
#12663=CARTESIAN_POINT ( 'NONE',  ( -0.001863919267159286786, 4.559812086079793048, -2.908070964936878333 ) ) ;
#12740=FACE_OUTER_BOUND ( 'NONE', #14931, .T. ) ;
#12763=VECTOR ( 'NONE', #13690, 39.37007874015748854 ) ;
#12864=EDGE_CURVE ( 'NONE', #19381, #644, #7073, .T. ) ;
#12925=DIRECTION ( 'NONE',  ( -0.8660254037844443697, 0.000000000000000000, 0.4999999999999902300 ) ) ;
#12977=VECTOR ( 'NONE', #12925, 39.37007874015747433 ) ;
#13001=CARTESIAN_POINT ( 'NONE',  ( -0.1166234456863257940, 4.111524471938507119, -2.802594437230254254 ) ) ;
#13026=ADVANCED_FACE ( 'NONE', ( #916 ), #8345, .T. ) ;
#13040=CARTESIAN_POINT ( 'NONE',  ( 0.2730879860166738338, 4.111524471938507119, -3.027594437230249902 ) ) ;
#13045=VECTOR ( 'NONE', #22279, 39.37007874015748854 ) ;
#13049=CARTESIAN_POINT ( 'NONE',  ( -0.1060554323913378977, 1.041821957232212270, -2.874935959385435336 ) ) ;
#13056=DIRECTION ( 'NONE',  ( 0.8660254037844433705, -9.889024645172693219E-32, -0.4999999999999916733 ) ) ;
#13075=EDGE_CURVE ( 'NONE', #18643, #11465, #4933, .T. ) ;
#13261=DIRECTION ( 'NONE',  ( 0.000000000000000000, 0.000000000000000000, -1.000000000000000000 ) ) ;
#13281=CARTESIAN_POINT ( 'NONE',  ( -0.001863919267159286786, 1.041821957232212270, -2.908070964936878333 ) ) ;
#13339=LINE ( 'NONE', #6242, #14013 ) ;
#13350=CARTESIAN_POINT ( 'NONE',  ( -0.5116234456863258950, 4.730490217694243604, -2.640781157734872320 ) ) ;
#13393=CARTESIAN_POINT ( 'NONE',  ( -0.1166234456863257940, 4.111524471938507119, -2.802594437230254254 ) ) ;
#13476=CARTESIAN_POINT ( 'NONE',  ( -0.3466234456863258040, 5.071846480923144718, -2.736043952151160141 ) ) ;
#13530=ORIENTED_EDGE ( 'NONE', *, *, #20801, .T. ) ;
#13548=CARTESIAN_POINT ( 'NONE',  ( -0.5116234456863258950, 4.559812086079793048, -2.813986238491759551 ) ) ;
#13577=CARTESIAN_POINT ( 'NONE',  ( -0.5116234456863258950, 4.111524471938507119, -3.001780280100677434 ) ) ;
#13690=DIRECTION ( 'NONE',  ( 0.8660254037844443697, 0.000000000000000000, -0.4999999999999901745 ) ) ;
#13692=DIRECTION ( 'NONE',  ( 0.4999999999999941158, 0.000000000000000000, 0.8660254037844420383 ) ) ;
#13695=PLANE ( 'NONE',  #19610 ) ;
#13712=CARTESIAN_POINT ( 'NONE',  ( -0.5116234456863258950, 4.901168349308694161, -2.640781157734872320 ) ) ;
#13732=EDGE_LOOP ( 'NONE', ( #19181, #1646, #675, #2812 ) ) ;
#13849=EDGE_CURVE ( 'NONE', #21597, #5324, #17819, .T. ) ;
#13890=CARTESIAN_POINT ( 'NONE',  ( -0.5116234456863258950, 1.999640111863030256, -2.727383698113316157 ) ) ;
#13973=CARTESIAN_POINT ( 'NONE',  ( 0.7108475124358382136, 4.111524471938507119, -3.019372695974962717 ) ) ;
#13979=ORIENTED_EDGE ( 'NONE', *, *, #17650, .T. ) ;
#14013=VECTOR ( 'NONE', #21123, 39.37007874015748854 ) ;
#14056=ORIENTED_EDGE ( 'NONE', *, *, #3010, .T. ) ;
#14139=EDGE_CURVE ( 'NONE', #2535, #9833, #9146, .T. ) ;
#14187=FACE_OUTER_BOUND ( 'NONE', #1152, .T. ) ;
#14288=ORIENTED_EDGE ( 'NONE', *, *, #18638, .F. ) ;
#14310=DIRECTION ( 'NONE',  ( -0.8660254037844437036, 0.000000000000000000, 0.4999999999999913403 ) ) ;
#14315=EDGE_CURVE ( 'NONE', #20728, #8276, #16322, .T. ) ;
#14323=ORIENTED_EDGE ( 'NONE', *, *, #4532, .F. ) ;
#14411=LINE ( 'NONE', #10873, #21526 ) ;
#14422=ADVANCED_FACE ( 'NONE', ( #20095 ), #18383, .T. ) ;
#14425=ORIENTED_EDGE ( 'NONE', *, *, #14139, .T. ) ;
#14441=LINE ( 'NONE', #21221, #574 ) ;
#14450=AXIS2_PLACEMENT_3D ( 'NONE', #2429, #9994, #17298 ) ;
#14453=EDGE_CURVE ( 'NONE', #4326, #11465, #14978, .T. ) ;
#14470=CARTESIAN_POINT ( 'NONE',  ( 0.3003475124358450099, 4.111524471938507119, -3.730379552481990491 ) ) ;
#14510=CARTESIAN_POINT ( 'NONE',  ( -0.4316174467094646694, 1.999640111863030256, -2.863205824962447021 ) ) ;
#14516=LINE ( 'NONE', #12576, #10802 ) ;
#14555=EDGE_CURVE ( 'NONE', #10744, #9500, #22523, .T. ) ;
#14598=ORIENTED_EDGE ( 'NONE', *, *, #18638, .T. ) ;
#14625=DIRECTION ( 'NONE',  ( -0.8660254037844420383, 0.000000000000000000, 0.4999999999999942268 ) ) ;
#14705=VECTOR ( 'NONE', #8141, 39.37007874015748854 ) ;
#14801=DIRECTION ( 'NONE',  ( 0.8660254037844384856, 0.000000000000000000, -0.5000000000000003331 ) ) ;
#14819=VECTOR ( 'NONE', #10396, 39.37007874015748854 ) ;
#14856=VECTOR ( 'NONE', #18089, 39.37007874015748143 ) ;
#14862=CARTESIAN_POINT ( 'NONE',  ( 0.3860879860166684940, 4.111524471938507119, -2.831872695974971599 ) ) ;
#14864=DIRECTION ( 'NONE',  ( 0.5000000000000005551, -0.000000000000000000, 0.8660254037844383745 ) ) ;
#14882=LINE ( 'NONE', #10739, #17786 ) ;
#14928=DIRECTION ( 'NONE',  ( 0.4999999999999918954, 0.000000000000000000, 0.8660254037844432595 ) ) ;
#14931=EDGE_LOOP ( 'NONE', ( #22796, #1844, #4293, #12266 ) ) ;
#14949=ADVANCED_FACE ( 'NONE', ( #11338 ), #11095, .T. ) ;
#14958=EDGE_LOOP ( 'NONE', ( #15608, #15343, #16599, #5532 ) ) ;
#14978=LINE ( 'NONE', #13040, #19479 ) ;
#15005=ADVANCED_FACE ( 'NONE', ( #9871 ), #19242, .T. ) ;
#15014=CARTESIAN_POINT ( 'NONE',  ( 0.2730879860166738338, 4.111524471938507119, -3.027594437230249902 ) ) ;
#15057=PLANE ( 'NONE',  #9677 ) ;
#15077=( BOUNDED_CURVE ( )  B_SPLINE_CURVE ( 2, ( #5848, #17195, #18904 ),
 .UNSPECIFIED., .F., .F. ) 
 B_SPLINE_CURVE_WITH_KNOTS ( ( 3, 3 ),
 ( 1.734723475976807094E-18, 0.002646478566469968440 ),
 .UNSPECIFIED. ) 
 CURVE ( )  GEOMETRIC_REPRESENTATION_ITEM ( )  RATIONAL_B_SPLINE_CURVE ( ( 1.000000000000000000, 0.4999999999999997780, 1.000000000000000000 ) ) 
 REPRESENTATION_ITEM ( '' )  );
#15101=LINE ( 'NONE', #2293, #18974 ) ;
#15181=AXIS2_PLACEMENT_3D ( 'NONE', #13049, #14625, #1571 ) ;
#15215=DIRECTION ( 'NONE',  ( -0.8660254037844377084, 0.000000000000000000, 0.5000000000000015543 ) ) ;
#15218=B_SPLINE_CURVE_WITH_KNOTS ( 'NONE', 3,
 ( #8489, #15931, #4829, #12299 ),
 .UNSPECIFIED., .F., .F.,
 ( 4, 4 ),
 ( 0.02432858112762280312, 0.08935694927272851140 ),
 .UNSPECIFIED. ) ;
#15231=VECTOR ( 'NONE', #7576, 39.37007874015748143 ) ;
#15343=ORIENTED_EDGE ( 'NONE', *, *, #3784, .F. ) ;
#15411=CARTESIAN_POINT ( 'NONE',  ( -0.4116234456863258617, 2.853030769935284372, -2.698516184653834582 ) ) ;
#15446=CARTESIAN_POINT ( 'NONE',  ( -0.5116234456863258950, 4.559812086079793048, -2.640781157734871876 ) ) ;
#15593=CARTESIAN_POINT ( 'NONE',  ( 0.7108475124358387687, 1.999640111863030700, -2.834606755790658461 ) ) ;
#15608=ORIENTED_EDGE ( 'NONE', *, *, #17515, .F. ) ;
#15609=ORIENTED_EDGE ( 'NONE', *, *, #11555, .T. ) ;
#15614=CARTESIAN_POINT ( 'NONE',  ( -0.5116234456863258950, 4.559812086079793048, -2.813986238491759551 ) ) ;
#15623=CARTESIAN_POINT ( 'NONE',  ( -0.1060554323913378977, 4.559812086079793048, -2.874935959385435336 ) ) ;
#15688=CARTESIAN_POINT ( 'NONE',  ( 0.7108475124358382136, 4.111524471938507119, -3.019372695974962717 ) ) ;
#15739=AXIS2_PLACEMENT_3D ( 'NONE', #8935, #23792, #23552 ) ;
#15791=ORIENTED_EDGE ( 'NONE', *, *, #21215, .T. ) ;
#15878=CARTESIAN_POINT ( 'NONE',  ( 0.000000000000000000, 0.000000000000000000, 0.000000000000000000 ) ) ;
#15897=CARTESIAN_POINT ( 'NONE',  ( 0.2730879860166738338, 1.999640111863030478, -2.842828497045944758 ) ) ;
#15931=CARTESIAN_POINT ( 'NONE',  ( -0.5116234456863258950, 2.853030769935285260, -2.756251211572797288 ) ) ;
#15983=CARTESIAN_POINT ( 'NONE',  ( -0.7171867353193159822, 1.999640111863030256, -2.958139940446594007 ) ) ;
#15993=AXIS2_PLACEMENT_3D ( 'NONE', #3409, #22181, #10859 ) ;
#16010=ORIENTED_EDGE ( 'NONE', *, *, #3068, .T. ) ;
#16016=EDGE_CURVE ( 'NONE', #12281, #18643, #1441, .T. ) ;
#16031=ORIENTED_EDGE ( 'NONE', *, *, #6337, .F. ) ;
#16065=VECTOR ( 'NONE', #8875, 39.37007874015748143 ) ;
#16159=ORIENTED_EDGE ( 'NONE', *, *, #12864, .F. ) ;
#16175=EDGE_CURVE ( 'NONE', #17621, #23261, #16806, .T. ) ;
#16261=DIRECTION ( 'NONE',  ( -0.8660254037844434816, 0.000000000000000000, 0.4999999999999915068 ) ) ;
#16297=AXIS2_PLACEMENT_3D ( 'NONE', #6642, #21640, #10558 ) ;
#16300=EDGE_LOOP ( 'NONE', ( #18262, #16995, #15609, #9033, #14425, #10795, #9195, #819, #20755, #13530, #2243 ) ) ;
#16322=( BOUNDED_CURVE ( )  B_SPLINE_CURVE ( 2, ( #13548, #17063, #5959 ),
 .UNSPECIFIED., .F., .T. ) 
 B_SPLINE_CURVE_WITH_KNOTS ( ( 3, 3 ),
 ( 0.000000000000000000, 0.005292957132939932544 ),
 .UNSPECIFIED. ) 
 CURVE ( )  GEOMETRIC_REPRESENTATION_ITEM ( )  RATIONAL_B_SPLINE_CURVE ( ( 1.000000000000000000, 0.4999999999999997780, 1.000000000000000000 ) ) 
 REPRESENTATION_ITEM ( '' )  );
#16328=CARTESIAN_POINT ( 'NONE',  ( 0.7108475124358382136, 4.111524471938507119, -3.019372695974962717 ) ) ;
#16359=CARTESIAN_POINT ( 'NONE',  ( 0.08808798601667688910, 4.111524471938507119, -3.348023836630494632 ) ) ;
#16363=VECTOR ( 'NONE', #20059, 39.37007874015748854 ) ;
#16366=( NAMED_UNIT ( * ) SI_UNIT ( $, .STERADIAN. ) SOLID_ANGLE_UNIT ( ) );
#16381=EDGE_CURVE ( 'NONE', #17621, #4265, #23107, .T. ) ;
#16393=DIRECTION ( 'NONE',  ( 0.000000000000000000, -1.000000000000000000, 0.000000000000000000 ) ) ;
#16566=DIRECTION ( 'NONE',  ( 0.000000000000000000, -0.9961946980917454342, 0.08715574274765845730 ) ) ;
#16590=CARTESIAN_POINT ( 'NONE',  ( 0.008081987039816235924, 1.999640111863030256, -3.301832351584418568 ) ) ;
#16599=ORIENTED_EDGE ( 'NONE', *, *, #20194, .T. ) ;
#16604=( LENGTH_UNIT ( ) NAMED_UNIT ( * ) SI_UNIT ( $, .METRE. ) );
#16705=VERTEX_POINT ( 'NONE', #14470 ) ;
#16714=CARTESIAN_POINT ( 'NONE',  ( -0.001863919267159286786, 4.559812086079793048, -2.908070964936878333 ) ) ;
#16746=DIRECTION ( 'NONE',  ( 0.8660254037844434816, 0.000000000000000000, -0.4999999999999915068 ) ) ;
#16762=VERTEX_POINT ( 'NONE', #7270 ) ;
#16795=VECTOR ( 'NONE', #8819, 39.37007874015748143 ) ;
#16806=LINE ( 'NONE', #9241, #12977 ) ;
#16992=CARTESIAN_POINT ( 'NONE',  ( -0.3616234456863258173, 4.559812086079793048, -2.727383698113316157 ) ) ;
#16995=ORIENTED_EDGE ( 'NONE', *, *, #4532, .T. ) ;
#17063=CARTESIAN_POINT ( 'NONE',  ( -0.5116234456863258950, 4.559812086079788607, -2.640781157734871876 ) ) ;
#17120=CARTESIAN_POINT ( 'NONE',  ( -0.5116234456863258950, 4.559812086079793048, -2.640781157734872320 ) ) ;
#17195=CARTESIAN_POINT ( 'NONE',  ( -0.5116234456863258950, 1.999640111863039582, -2.640781157734871876 ) ) ;
#17298=DIRECTION ( 'NONE',  ( 0.000000000000000000, -0.000000000000000000, 1.000000000000000000 ) ) ;
#17333=LINE ( 'NONE', #627, #2565 ) ;
#17372=CARTESIAN_POINT ( 'NONE',  ( -0.1166234456863257940, 4.111524471938507119, -2.802594437230254254 ) ) ;
#17471=AXIS2_PLACEMENT_3D ( 'NONE', #621, #9897, #9529 ) ;
#17474=CARTESIAN_POINT ( 'NONE',  ( -0.5116234456863258950, 1.828961980248579033, -2.640781157734872320 ) ) ;
#17515=EDGE_CURVE ( 'NONE', #4879, #2744, #14411, .T. ) ;
#17527=ORIENTED_EDGE ( 'NONE', *, *, #6337, .T. ) ;
#17531=UNCERTAINTY_MEASURE_WITH_UNIT (LENGTH_MEASURE( 1.000000000000000082E-05 ), #20141, 'distance_accuracy_value', 'NONE');
#17557=ADVANCED_FACE ( 'NONE', ( #18184 ), #8917, .T. ) ;
#17597=ORIENTED_EDGE ( 'NONE', *, *, #13849, .F. ) ;
#17621=VERTEX_POINT ( 'NONE', #7804 ) ;
#17639=DIRECTION ( 'NONE',  ( -0.4999999999999942268, 0.000000000000000000, -0.8660254037844420383 ) ) ;
#17650=EDGE_CURVE ( 'NONE', #8276, #9492, #18775, .T. ) ;
#17673=ORIENTED_EDGE ( 'NONE', *, *, #2339, .F. ) ;
#17715=ORIENTED_EDGE ( 'NONE', *, *, #20172, .F. ) ;
#17724=CARTESIAN_POINT ( 'NONE',  ( -0.02441201398332129568, 4.111524471938507119, -3.542879552481994043 ) ) ;
#17729=LINE ( 'NONE', #10544, #16795 ) ;
#17760=DIRECTION ( 'NONE',  ( 0.000000000000000000, -0.9961946980917454342, 0.08715574274765833240 ) ) ;
#17777=CARTESIAN_POINT ( 'NONE',  ( 0.08808798601667681971, 1.999640111863030256, -3.163257896446189488 ) ) ;
#17786=VECTOR ( 'NONE', #23638, 39.37007874015748143 ) ;
#17789=DIRECTION ( 'NONE',  ( -0.8651979924482661177, 0.04370253788966847741, 0.4995222938423191095 ) ) ;
#17819=LINE ( 'NONE', #18178, #14819 ) ;
#17878=ORIENTED_EDGE ( 'NONE', *, *, #16175, .F. ) ;
#17931=SHAPE_REPRESENTATION ( 'Aloris-BXA-Wedge-L', ( #9127 ), #2138 ) ;
#18019=VERTEX_POINT ( 'NONE', #15623 ) ;
#18065=SHAPE_REPRESENTATION_RELATIONSHIP ( 'NONE' , 'NONE' ,  #17931, #7396 ) ;
#18089=DIRECTION ( 'NONE',  ( 0.000000000000000000, -0.9961946980917454342, 0.08715574274765833240 ) ) ;
#18099=PRODUCT ( 'Aloris-BXA-Wedge-L', 'Aloris-BXA-Wedge-L', '', ( #12157 ) ) ;
#18106=FACE_OUTER_BOUND ( 'NONE', #11810, .T. ) ;
#18178=CARTESIAN_POINT ( 'NONE',  ( 0.08808798601667688910, 4.111524471938507119, -3.348023836630494632 ) ) ;
#18184=FACE_OUTER_BOUND ( 'NONE', #13732, .T. ) ;
#18185=ORIENTED_EDGE ( 'NONE', *, *, #11721, .T. ) ;
#18205=CARTESIAN_POINT ( 'NONE',  ( -0.02441201398332155936, 1.999640111863030256, -3.358113612297689343 ) ) ;
#18208=AXIS2_PLACEMENT_3D ( 'NONE', #17724, #19794, #16261 ) ;
#18216=CARTESIAN_POINT ( 'NONE',  ( 0.000000000000000000, 4.111524471938507119, -0.2004988538245859597 ) ) ;
#18262=ORIENTED_EDGE ( 'NONE', *, *, #8264, .T. ) ;
#18383=PLANE ( 'NONE',  #5854 ) ;
#18413=DIRECTION ( 'NONE',  ( 0.000000000000000000, -0.9961946980917454342, 0.08715574274765833240 ) ) ;
#18422=DIRECTION ( 'NONE',  ( 0.4999999999999930611, 0.000000000000000000, 0.8660254037844425934 ) ) ;
#18465=DIRECTION ( 'NONE',  ( -1.000000000000000000, 0.000000000000000000, -0.000000000000000000 ) ) ;
#18540=DIRECTION ( 'NONE',  ( -0.8651979924482653406, 0.04370253788966859537, 0.4995222938423205528 ) ) ;
#18563=DIRECTION ( 'NONE',  ( -0.5000000000000003331, 0.000000000000000000, -0.8660254037844384856 ) ) ;
#18638=EDGE_CURVE ( 'NONE', #9500, #20728, #4913, .T. ) ;
#18643=VERTEX_POINT ( 'NONE', #5393 ) ;
#18679=ADVANCED_FACE ( 'NONE', ( #10650 ), #3443, .T. ) ;
#18728=ORIENTED_EDGE ( 'NONE', *, *, #2364, .T. ) ;
#18759=CARTESIAN_POINT ( 'NONE',  ( -0.1166234456863258218, 4.111524471938507119, -2.868834514064774854 ) ) ;
#18775=B_SPLINE_CURVE_WITH_KNOTS ( 'NONE', 3,
 ( #20726, #11714, #5736, #4023 ),
 .UNSPECIFIED., .F., .F.,
 ( 4, 4 ),
 ( 0.08935694927272852528, 0.1543853174178340670 ),
 .UNSPECIFIED. ) ;
#18882=ORIENTED_EDGE ( 'NONE', *, *, #12864, .T. ) ;
#18887=ADVANCED_FACE ( 'NONE', ( #4283 ), #13695, .T. ) ;
#18904=CARTESIAN_POINT ( 'NONE',  ( -0.5116234456863258950, 1.999640111863030256, -2.727383698113316157 ) ) ;
#18973=ORIENTED_EDGE ( 'NONE', *, *, #14453, .T. ) ;
#18974=VECTOR ( 'NONE', #5817, 39.37007874015748854 ) ;
#18975=ORIENTED_EDGE ( 'NONE', *, *, #21038, .T. ) ;
#19042=LINE ( 'NONE', #380, #12763 ) ;
#19094=DIRECTION ( 'NONE',  ( 0.8660254037844382635, 0.000000000000000000, -0.5000000000000004441 ) ) ;
#19181=ORIENTED_EDGE ( 'NONE', *, *, #14139, .F. ) ;
#19242=PLANE ( 'NONE',  #14450 ) ;
#19305=EDGE_CURVE ( 'NONE', #9833, #4879, #8541, .T. ) ;
#19381=VERTEX_POINT ( 'NONE', #20720 ) ;
#19395=ORIENTED_EDGE ( 'NONE', *, *, #20172, .T. ) ;
#19458=ORIENTED_EDGE ( 'NONE', *, *, #2615, .F. ) ;
#19459=DIRECTION ( 'NONE',  ( 0.000000000000000000, -0.9961946980917454342, 0.08715574274765833240 ) ) ;
#19474=EDGE_CURVE ( 'NONE', #21597, #2535, #10988, .T. ) ;
#19479=VECTOR ( 'NONE', #1678, 39.37007874015748143 ) ;
#19550=LINE ( 'NONE', #21861, #8854 ) ;
#19576=LINE ( 'NONE', #15688, #20606 ) ;
#19610=AXIS2_PLACEMENT_3D ( 'NONE', #13577, #865, #10032 ) ;
#19675=DIRECTION ( 'NONE',  ( 0.000000000000000000, -0.000000000000000000, -1.000000000000000000 ) ) ;
#19715=DIRECTION ( 'NONE',  ( -0.5000000000000003331, 0.000000000000000000, -0.8660254037844384856 ) ) ;
#19724=ORIENTED_EDGE ( 'NONE', *, *, #16016, .F. ) ;
#19743=EDGE_CURVE ( 'NONE', #12281, #4326, #20576, .T. ) ;
#19794=DIRECTION ( 'NONE',  ( -0.4985709748471497393, -0.07555085810113111588, -0.8635502596144276621 ) ) ;
#19814=ORIENTED_EDGE ( 'NONE', *, *, #14453, .F. ) ;
#19850=VECTOR ( 'NONE', #13261, 39.37007874015748143 ) ;
#19937=VERTEX_POINT ( 'NONE', #13393 ) ;
#20059=DIRECTION ( 'NONE',  ( -0.4999999999999916733, -6.654928120984804281E-16, -0.8660254037844433705 ) ) ;
#20095=FACE_OUTER_BOUND ( 'NONE', #9224, .T. ) ;
#20141=( CONVERSION_BASED_UNIT ( 'INCH', #1366 ) LENGTH_UNIT ( ) NAMED_UNIT ( #577 ) );
#20172=EDGE_CURVE ( 'NONE', #8965, #12281, #7837, .T. ) ;
#20178=CARTESIAN_POINT ( 'NONE',  ( -0.5116234456863258950, 2.853030769935284372, -2.756251211572797288 ) ) ;
#20194=EDGE_CURVE ( 'NONE', #16705, #8965, #7599, .T. ) ;
#20269=ORIENTED_EDGE ( 'NONE', *, *, #9690, .T. ) ;
#20275=CARTESIAN_POINT ( 'NONE',  ( -0.5116234456863258950, 4.559812086079793048, -3.041000364337123507 ) ) ;
#20353=LINE ( 'NONE', #14510, #208 ) ;
#20410=VERTEX_POINT ( 'NONE', #12002 ) ;
#20483=CARTESIAN_POINT ( 'NONE',  ( 0.08808798601667688910, 4.111524471938507119, -3.348023836630494632 ) ) ;
#20576=LINE ( 'NONE', #14862, #13045 ) ;
#20606=VECTOR ( 'NONE', #19459, 39.37007874015748143 ) ;
#20720=CARTESIAN_POINT ( 'NONE',  ( -0.1166234456863257940, 1.999640111863030478, -2.868834514064774854 ) ) ;
#20726=CARTESIAN_POINT ( 'NONE',  ( -0.3616234456863257618, 4.559812086079793048, -2.727383698113316157 ) ) ;
#20728=VERTEX_POINT ( 'NONE', #15614 ) ;
#20755=ORIENTED_EDGE ( 'NONE', *, *, #13075, .T. ) ;
#20763=CARTESIAN_POINT ( 'NONE',  ( 0.7108475124358382136, 4.111524471938507119, -3.019372695974962717 ) ) ;
#20801=EDGE_CURVE ( 'NONE', #11465, #20410, #23385, .T. ) ;
#20808=ORIENTED_EDGE ( 'NONE', *, *, #23240, .F. ) ;
#20891=CARTESIAN_POINT ( 'NONE',  ( -0.5116234456863258950, 3.706421428007538488, -2.640781157734872320 ) ) ;
#21038=EDGE_CURVE ( 'NONE', #2739, #20728, #15218, .T. ) ;
#21044=LINE ( 'NONE', #15446, #23685 ) ;
#21123=DIRECTION ( 'NONE',  ( -0.8660254037844382635, 6.853229114107538658E-30, 0.5000000000000004441 ) ) ;
#21132=CARTESIAN_POINT ( 'NONE',  ( -0.3516234456863258084, 4.901168349308694161, -2.733157200805212295 ) ) ;
#21188=DESIGN_CONTEXT ( 'detailed design', #1411, 'design' ) ;
#21211=EDGE_LOOP ( 'NONE', ( #1845, #1730, #7565, #23665, #8155, #17715, #12485, #793, #17597, #8100, #7008, #7805 ) ) ;
#21215=EDGE_CURVE ( 'NONE', #23261, #16762, #14441, .T. ) ;
#21221=CARTESIAN_POINT ( 'NONE',  ( -0.09435543239133792337, 1.041821957232212270, -2.854670964936879329 ) ) ;
#21363=PLANE ( 'NONE',  #24043 ) ;
#21384=PLANE ( 'NONE',  #18208 ) ;
#21420=AXIS2_PLACEMENT_3D ( 'NONE', #13973, #4693, #12161 ) ;
#21436=LINE ( 'NONE', #10353, #14705 ) ;
#21526=VECTOR ( 'NONE', #3299, 39.37007874015748854 ) ;
#21597=VERTEX_POINT ( 'NONE', #21639 ) ;
#21639=CARTESIAN_POINT ( 'NONE',  ( 0.08808798601667688910, 4.111524471938507119, -3.348023836630494632 ) ) ;
#21640=DIRECTION ( 'NONE',  ( 0.4985709748471496838, 0.07555085810113111588, 0.8635502596144277732 ) ) ;
#21759=SHAPE_DEFINITION_REPRESENTATION ( #23527, #17931 ) ;
#21836=VECTOR ( 'NONE', #16746, 39.37007874015748854 ) ;
#21861=CARTESIAN_POINT ( 'NONE',  ( -0.5116234456863258950, 4.111524471938507119, -3.001780280100677434 ) ) ;
#21875=ORIENTED_EDGE ( 'NONE', *, *, #20801, .F. ) ;
#21899=CARTESIAN_POINT ( 'NONE',  ( -0.5116234456863258950, 4.559812086079793048, -3.041000364337123507 ) ) ;
#21904=LINE ( 'NONE', #12663, #12440 ) ;
#21923=PLANE ( 'NONE',  #15181 ) ;
#21937=DIRECTION ( 'NONE',  ( 0.8660254037844434816, 0.000000000000000000, -0.4999999999999916178 ) ) ;
#21998=FACE_OUTER_BOUND ( 'NONE', #8516, .T. ) ;
#22131=EDGE_CURVE ( 'NONE', #23062, #2535, #20353, .T. ) ;
#22181=DIRECTION ( 'NONE',  ( -1.000000000000000000, 0.000000000000000000, -0.000000000000000000 ) ) ;
#22279=DIRECTION ( 'NONE',  ( -0.4999999999999916178, 0.000000000000000000, -0.8660254037844433705 ) ) ;
#22348=CARTESIAN_POINT ( 'NONE',  ( 0.3003475124358450099, 4.111524471938507119, -3.730379552481990491 ) ) ;
#22419=ORIENTED_EDGE ( 'NONE', *, *, #7426, .F. ) ;
#22481=CARTESIAN_POINT ( 'NONE',  ( -0.5116234456863258950, 1.487605717019675700, -2.710063190037627745 ) ) ;
#22523=LINE ( 'NONE', #2291, #5456 ) ;
#22670=DIRECTION ( 'NONE',  ( -0.4999999999999931166, -6.654928120984804281E-16, -0.8660254037844425934 ) ) ;
#22796=ORIENTED_EDGE ( 'NONE', *, *, #3497, .F. ) ;
#22812=EDGE_LOOP ( 'NONE', ( #7866, #18975, #14288, #5485 ) ) ;
#22839=CARTESIAN_POINT ( 'NONE',  ( -0.5116234456863258950, 1.658283848634127366, -2.640781157734872320 ) ) ;
#22912=CARTESIAN_POINT ( 'NONE',  ( -0.02441201398332129568, 4.111524471938507119, -3.542879552481994043 ) ) ;
#22949=CARTESIAN_POINT ( 'NONE',  ( -0.5116234456863258950, 1.487605717019675700, -2.640781157734872320 ) ) ;
#23062=VERTEX_POINT ( 'NONE', #23945 ) ;
#23107=LINE ( 'NONE', #13281, #11389 ) ;
#23181=DIRECTION ( 'NONE',  ( 0.000000000000000000, 0.000000000000000000, 1.000000000000000000 ) ) ;
#23240=EDGE_CURVE ( 'NONE', #18019, #16762, #17333, .T. ) ;
#23257=CARTESIAN_POINT ( 'NONE',  ( 0.3860879860166684940, 4.111524471938507119, -2.831872695974971599 ) ) ;
#23261=VERTEX_POINT ( 'NONE', #10029 ) ;
#23265=AXIS2_PLACEMENT_3D ( 'NONE', #23257, #17789, #4618 ) ;
#23294=DIRECTION ( 'NONE',  ( 1.000000000000000000, 0.000000000000000000, 0.000000000000000000 ) ) ;
#23385=LINE ( 'NONE', #4861, #2149 ) ;
#23404=DIRECTION ( 'NONE',  ( 0.8660254037844434816, 0.000000000000000000, -0.4999999999999916178 ) ) ;
#23527=PRODUCT_DEFINITION_SHAPE ( 'NONE', 'NONE',  #8791 ) ;
#23552=DIRECTION ( 'NONE',  ( -0.4999999999999918954, 0.000000000000000000, -0.8660254037844432595 ) ) ;
#23573=PLANE ( 'NONE',  #16297 ) ;
#23629=VECTOR ( 'NONE', #14310, 39.37007874015748854 ) ;
#23638=DIRECTION ( 'NONE',  ( 0.000000000000000000, -0.9961946980917454342, 0.08715574274765833240 ) ) ;
#23650=CARTESIAN_POINT ( 'NONE',  ( -0.7171867353193159822, 1.999640111863030256, -2.958139940446594007 ) ) ;
#23665=ORIENTED_EDGE ( 'NONE', *, *, #3068, .F. ) ;
#23685=VECTOR ( 'NONE', #19094, 39.37007874015748854 ) ;
#23792=DIRECTION ( 'NONE',  ( 0.8651979924482660067, -0.04370253788966849823, -0.4995222938423193870 ) ) ;
#23867=CARTESIAN_POINT ( 'NONE',  ( -0.1060554323913378977, 1.041821957232212270, -2.874935959385435336 ) ) ;
#23940=CARTESIAN_POINT ( 'NONE',  ( -0.5116234456863258950, 5.071846480923144718, -2.831306746567448407 ) ) ;
#23945=CARTESIAN_POINT ( 'NONE',  ( -0.5116234456863258950, 1.999640111863029812, -2.817014339916372290 ) ) ;
#24043=AXIS2_PLACEMENT_3D ( 'NONE', #23650, #5124, #12590 ) ;
#24152=COLOUR_RGB('Sky Blue', 0.40784314, 0.44705882, 0.49803922);
#24153=FILL_AREA_STYLE_COLOUR('',#24152);
#24154=FILL_AREA_STYLE('',(#24153));
#24155=SURFACE_STYLE_FILL_AREA(#24154);
#24156=SURFACE_SIDE_STYLE('',(#24155));
#24157=SURFACE_STYLE_USAGE(.BOTH.,#24156);
#24158=PRESENTATION_STYLE_ASSIGNMENT((#24157));
#24184=STYLED_ITEM('',(#24158),#1208);
#24185=MECHANICAL_DESIGN_GEOMETRIC_PRESENTATION_REPRESENTATION('',(#24184),#2138);
ENDSEC;
END-ISO-10303-21;
